ISO-10303-21;
HEADER;
/* Generated by software containing ST-Developer
 * from STEP Tools, Inc. (www.steptools.com) 
 */

FILE_DESCRIPTION(
/* description */ ('Gravity roller conveyor section'),
/* implementation_level */ '2;1');

FILE_NAME(
/* name */ 'M5x14 Cap Screw.step',
/* time_stamp */ '2026-11-02T07:43:02-08:00',
/* author */ (''),
/* organization */ (''),
/* preprocessor_version */ 'ST-DEVELOPER v20.2',
/* originating_system */ 'Autodesk Translation Framework v15.17.0.0',
/* authorisation */ '');

FILE_SCHEMA (('AUTOMOTIVE_DESIGN { 1 0 10303 214 3 1 1 }'));
ENDSEC;

DATA;
#10=MECHANICAL_DESIGN_GEOMETRIC_PRESENTATION_REPRESENTATION('',(#569),#13821);
#422=CONICAL_SURFACE('',#8693,0.4,0.785398163397448);
#423=CONICAL_SURFACE('',#8697,0.41,0.785398163397448);
#424=CONICAL_SURFACE('',#8701,0.26,0.463647609000806);
#428=ORIENTED_CLOSED_SHELL('',*,#7670,.F.);
#432=BREP_WITH_VOIDS('Body1',#7671,(#428));
#493=SHAPE_REPRESENTATION_RELATIONSHIP('SRR','None',#14032,#527);
#527=ADVANCED_BREP_SHAPE_REPRESENTATION('',(#432),#13819);
#569=STYLED_ITEM('',(#14193),#432);
#693=FACE_BOUND('',#1914,.T.);
#988=PLANE('',#8681);
#989=PLANE('',#8682);
#990=PLANE('',#8683);
#991=PLANE('',#8684);
#992=PLANE('',#8685);
#993=PLANE('',#8686);
#994=PLANE('',#8687);
#995=PLANE('',#8688);
#996=PLANE('',#8689);
#997=PLANE('',#8691);
#998=PLANE('',#8699);
#1397=FACE_OUTER_BOUND('',#1900,.T.);
#1398=FACE_OUTER_BOUND('',#1901,.T.);
#1399=FACE_OUTER_BOUND('',#1902,.T.);
#1400=FACE_OUTER_BOUND('',#1903,.T.);
#1401=FACE_OUTER_BOUND('',#1904,.T.);
#1402=FACE_OUTER_BOUND('',#1905,.T.);
#1403=FACE_OUTER_BOUND('',#1906,.T.);
#1404=FACE_OUTER_BOUND('',#1907,.T.);
#1405=FACE_OUTER_BOUND('',#1908,.T.);
#1406=FACE_OUTER_BOUND('',#1909,.T.);
#1407=FACE_OUTER_BOUND('',#1910,.T.);
#1408=FACE_OUTER_BOUND('',#1911,.T.);
#1409=FACE_OUTER_BOUND('',#1912,.T.);
#1410=FACE_OUTER_BOUND('',#1913,.T.);
#1411=FACE_OUTER_BOUND('',#1915,.T.);
#1412=FACE_OUTER_BOUND('',#1916,.T.);
#1900=EDGE_LOOP('',(#7016,#7017,#7018,#7019));
#1901=EDGE_LOOP('',(#7020,#7021,#7022,#7023));
#1902=EDGE_LOOP('',(#7024,#7025,#7026,#7027));
#1903=EDGE_LOOP('',(#7028,#7029,#7030,#7031));
#1904=EDGE_LOOP('',(#7032,#7033,#7034,#7035));
#1905=EDGE_LOOP('',(#7036,#7037,#7038,#7039));
#1906=EDGE_LOOP('',(#7040,#7041,#7042,#7043,#7044,#7045));
#1907=EDGE_LOOP('',(#7046,#7047,#7048,#7049,#7050,#7051));
#1908=EDGE_LOOP('',(#7052));
#1909=EDGE_LOOP('',(#7053));
#1910=EDGE_LOOP('',(#7054,#7055,#7056,#7057));
#1911=EDGE_LOOP('',(#7058,#7059,#7060,#7061));
#1912=EDGE_LOOP('',(#7062,#7063,#7064,#7065));
#1913=EDGE_LOOP('',(#7066));
#1914=EDGE_LOOP('',(#7067));
#1915=EDGE_LOOP('',(#7068,#7069,#7070,#7071));
#1916=EDGE_LOOP('',(#7072,#7073,#7074,#7075));
#2616=LINE('',#13534,#3334);
#2617=LINE('',#13536,#3335);
#2618=LINE('',#13538,#3336);
#2619=LINE('',#13539,#3337);
#2620=LINE('',#13542,#3338);
#2621=LINE('',#13544,#3339);
#2622=LINE('',#13545,#3340);
#2623=LINE('',#13548,#3341);
#2624=LINE('',#13550,#3342);
#2625=LINE('',#13551,#3343);
#2626=LINE('',#13554,#3344);
#2627=LINE('',#13556,#3345);
#2628=LINE('',#13557,#3346);
#2629=LINE('',#13560,#3347);
#2630=LINE('',#13562,#3348);
#2631=LINE('',#13563,#3349);
#2632=LINE('',#13565,#3350);
#2633=LINE('',#13566,#3351);
#2634=LINE('',#13578,#3352);
#2635=LINE('',#13582,#3353);
#2636=LINE('',#13586,#3354);
#2637=LINE('',#13593,#3355);
#2638=LINE('',#13595,#3356);
#3334=VECTOR('',#10763,1.);
#3335=VECTOR('',#10764,1.);
#3336=VECTOR('',#10765,1.);
#3337=VECTOR('',#10766,1.);
#3338=VECTOR('',#10769,1.);
#3339=VECTOR('',#10770,1.);
#3340=VECTOR('',#10771,1.);
#3341=VECTOR('',#10774,1.);
#3342=VECTOR('',#10775,1.);
#3343=VECTOR('',#10776,1.);
#3344=VECTOR('',#10779,1.);
#3345=VECTOR('',#10780,1.);
#3346=VECTOR('',#10781,1.);
#3347=VECTOR('',#10784,1.);
#3348=VECTOR('',#10785,1.);
#3349=VECTOR('',#10786,1.);
#3350=VECTOR('',#10789,1.);
#3351=VECTOR('',#10790,1.);
#3352=VECTOR('',#10807,0.4);
#3353=VECTOR('',#10812,0.425);
#3354=VECTOR('',#10817,0.41);
#3355=VECTOR('',#10826,0.26);
#3356=VECTOR('',#10829,0.25);
#3573=CIRCLE('',#8690,0.24505);
#3574=CIRCLE('',#8692,0.375);
#3575=CIRCLE('',#8694,0.425);
#3576=CIRCLE('',#8696,0.425);
#3577=CIRCLE('',#8698,0.395);
#3578=CIRCLE('',#8700,0.27);
#3579=CIRCLE('',#8702,0.24505);
#4201=VERTEX_POINT('',#13532);
#4202=VERTEX_POINT('',#13533);
#4203=VERTEX_POINT('',#13535);
#4204=VERTEX_POINT('',#13537);
#4205=VERTEX_POINT('',#13541);
#4206=VERTEX_POINT('',#13543);
#4207=VERTEX_POINT('',#13547);
#4208=VERTEX_POINT('',#13549);
#4209=VERTEX_POINT('',#13553);
#4210=VERTEX_POINT('',#13555);
#4211=VERTEX_POINT('',#13559);
#4212=VERTEX_POINT('',#13561);
#4213=VERTEX_POINT('',#13570);
#4214=VERTEX_POINT('',#13573);
#4215=VERTEX_POINT('',#13576);
#4216=VERTEX_POINT('',#13580);
#4217=VERTEX_POINT('',#13584);
#4218=VERTEX_POINT('',#13588);
#4219=VERTEX_POINT('',#13591);
#5145=EDGE_CURVE('',#4201,#4202,#2616,.T.);
#5146=EDGE_CURVE('',#4202,#4203,#2617,.T.);
#5147=EDGE_CURVE('',#4203,#4204,#2618,.T.);
#5148=EDGE_CURVE('',#4201,#4204,#2619,.T.);
#5149=EDGE_CURVE('',#4202,#4205,#2620,.T.);
#5150=EDGE_CURVE('',#4205,#4206,#2621,.T.);
#5151=EDGE_CURVE('',#4206,#4203,#2622,.T.);
#5152=EDGE_CURVE('',#4205,#4207,#2623,.T.);
#5153=EDGE_CURVE('',#4207,#4208,#2624,.T.);
#5154=EDGE_CURVE('',#4208,#4206,#2625,.T.);
#5155=EDGE_CURVE('',#4207,#4209,#2626,.T.);
#5156=EDGE_CURVE('',#4209,#4210,#2627,.T.);
#5157=EDGE_CURVE('',#4210,#4208,#2628,.T.);
#5158=EDGE_CURVE('',#4209,#4211,#2629,.T.);
#5159=EDGE_CURVE('',#4211,#4212,#2630,.T.);
#5160=EDGE_CURVE('',#4212,#4210,#2631,.T.);
#5161=EDGE_CURVE('',#4211,#4201,#2632,.T.);
#5162=EDGE_CURVE('',#4204,#4212,#2633,.T.);
#5163=EDGE_CURVE('',#4213,#4213,#3573,.T.);
#5164=EDGE_CURVE('',#4214,#4214,#3574,.T.);
#5165=EDGE_CURVE('',#4215,#4215,#3575,.T.);
#5166=EDGE_CURVE('',#4215,#4214,#2634,.T.);
#5167=EDGE_CURVE('',#4216,#4216,#3576,.T.);
#5168=EDGE_CURVE('',#4216,#4215,#2635,.T.);
#5169=EDGE_CURVE('',#4217,#4217,#3577,.T.);
#5170=EDGE_CURVE('',#4217,#4216,#2636,.T.);
#5171=EDGE_CURVE('',#4218,#4218,#3578,.T.);
#5172=EDGE_CURVE('',#4219,#4219,#3579,.F.);
#5173=EDGE_CURVE('',#4219,#4218,#2637,.T.);
#5174=EDGE_CURVE('',#4213,#4219,#2638,.T.);
#7016=ORIENTED_EDGE('',*,*,#5145,.T.);
#7017=ORIENTED_EDGE('',*,*,#5146,.T.);
#7018=ORIENTED_EDGE('',*,*,#5147,.T.);
#7019=ORIENTED_EDGE('',*,*,#5148,.F.);
#7020=ORIENTED_EDGE('',*,*,#5149,.T.);
#7021=ORIENTED_EDGE('',*,*,#5150,.T.);
#7022=ORIENTED_EDGE('',*,*,#5151,.T.);
#7023=ORIENTED_EDGE('',*,*,#5146,.F.);
#7024=ORIENTED_EDGE('',*,*,#5152,.T.);
#7025=ORIENTED_EDGE('',*,*,#5153,.T.);
#7026=ORIENTED_EDGE('',*,*,#5154,.T.);
#7027=ORIENTED_EDGE('',*,*,#5150,.F.);
#7028=ORIENTED_EDGE('',*,*,#5155,.T.);
#7029=ORIENTED_EDGE('',*,*,#5156,.T.);
#7030=ORIENTED_EDGE('',*,*,#5157,.T.);
#7031=ORIENTED_EDGE('',*,*,#5153,.F.);
#7032=ORIENTED_EDGE('',*,*,#5158,.T.);
#7033=ORIENTED_EDGE('',*,*,#5159,.T.);
#7034=ORIENTED_EDGE('',*,*,#5160,.T.);
#7035=ORIENTED_EDGE('',*,*,#5156,.F.);
#7036=ORIENTED_EDGE('',*,*,#5161,.T.);
#7037=ORIENTED_EDGE('',*,*,#5148,.T.);
#7038=ORIENTED_EDGE('',*,*,#5162,.T.);
#7039=ORIENTED_EDGE('',*,*,#5159,.F.);
#7040=ORIENTED_EDGE('',*,*,#5161,.F.);
#7041=ORIENTED_EDGE('',*,*,#5158,.F.);
#7042=ORIENTED_EDGE('',*,*,#5155,.F.);
#7043=ORIENTED_EDGE('',*,*,#5152,.F.);
#7044=ORIENTED_EDGE('',*,*,#5149,.F.);
#7045=ORIENTED_EDGE('',*,*,#5145,.F.);
#7046=ORIENTED_EDGE('',*,*,#5162,.F.);
#7047=ORIENTED_EDGE('',*,*,#5147,.F.);
#7048=ORIENTED_EDGE('',*,*,#5151,.F.);
#7049=ORIENTED_EDGE('',*,*,#5154,.F.);
#7050=ORIENTED_EDGE('',*,*,#5157,.F.);
#7051=ORIENTED_EDGE('',*,*,#5160,.F.);
#7052=ORIENTED_EDGE('',*,*,#5163,.F.);
#7053=ORIENTED_EDGE('',*,*,#5164,.F.);
#7054=ORIENTED_EDGE('',*,*,#5165,.F.);
#7055=ORIENTED_EDGE('',*,*,#5166,.T.);
#7056=ORIENTED_EDGE('',*,*,#5164,.T.);
#7057=ORIENTED_EDGE('',*,*,#5166,.F.);
#7058=ORIENTED_EDGE('',*,*,#5167,.F.);
#7059=ORIENTED_EDGE('',*,*,#5168,.T.);
#7060=ORIENTED_EDGE('',*,*,#5165,.T.);
#7061=ORIENTED_EDGE('',*,*,#5168,.F.);
#7062=ORIENTED_EDGE('',*,*,#5169,.F.);
#7063=ORIENTED_EDGE('',*,*,#5170,.T.);
#7064=ORIENTED_EDGE('',*,*,#5167,.T.);
#7065=ORIENTED_EDGE('',*,*,#5170,.F.);
#7066=ORIENTED_EDGE('',*,*,#5169,.T.);
#7067=ORIENTED_EDGE('',*,*,#5171,.F.);
#7068=ORIENTED_EDGE('',*,*,#5172,.F.);
#7069=ORIENTED_EDGE('',*,*,#5173,.T.);
#7070=ORIENTED_EDGE('',*,*,#5171,.T.);
#7071=ORIENTED_EDGE('',*,*,#5173,.F.);
#7072=ORIENTED_EDGE('',*,*,#5163,.T.);
#7073=ORIENTED_EDGE('',*,*,#5174,.T.);
#7074=ORIENTED_EDGE('',*,*,#5172,.T.);
#7075=ORIENTED_EDGE('',*,*,#5174,.F.);
#7201=CYLINDRICAL_SURFACE('',#8695,0.425);
#7202=CYLINDRICAL_SURFACE('',#8703,0.24505);
#7598=ADVANCED_FACE('',(#1397),#988,.F.);
#7599=ADVANCED_FACE('',(#1398),#989,.F.);
#7600=ADVANCED_FACE('',(#1399),#990,.F.);
#7601=ADVANCED_FACE('',(#1400),#991,.F.);
#7602=ADVANCED_FACE('',(#1401),#992,.F.);
#7603=ADVANCED_FACE('',(#1402),#993,.F.);
#7604=ADVANCED_FACE('',(#1403),#994,.F.);
#7605=ADVANCED_FACE('',(#1404),#995,.F.);
#7606=ADVANCED_FACE('',(#1405),#996,.F.);
#7607=ADVANCED_FACE('',(#1406),#997,.T.);
#7608=ADVANCED_FACE('',(#1407),#422,.T.);
#7609=ADVANCED_FACE('',(#1408),#7201,.T.);
#7610=ADVANCED_FACE('',(#1409),#423,.T.);
#7611=ADVANCED_FACE('',(#1410,#693),#998,.T.);
#7612=ADVANCED_FACE('',(#1411),#424,.T.);
#7613=ADVANCED_FACE('',(#1412),#7202,.T.);
#7670=CLOSED_SHELL('',(#7598,#7599,#7600,#7601,#7602,#7603,#7604,#7605));
#7671=CLOSED_SHELL('',(#7606,#7607,#7608,#7609,#7610,#7611,#7612,#7613));
#8680=AXIS2_PLACEMENT_3D('',#13530,#10759,#10760);
#8681=AXIS2_PLACEMENT_3D('',#13531,#10761,#10762);
#8682=AXIS2_PLACEMENT_3D('',#13540,#10767,#10768);
#8683=AXIS2_PLACEMENT_3D('',#13546,#10772,#10773);
#8684=AXIS2_PLACEMENT_3D('',#13552,#10777,#10778);
#8685=AXIS2_PLACEMENT_3D('',#13558,#10782,#10783);
#8686=AXIS2_PLACEMENT_3D('',#13564,#10787,#10788);
#8687=AXIS2_PLACEMENT_3D('',#13567,#10791,#10792);
#8688=AXIS2_PLACEMENT_3D('',#13568,#10793,#10794);
#8689=AXIS2_PLACEMENT_3D('',#13569,#10795,#10796);
#8690=AXIS2_PLACEMENT_3D('',#13571,#10797,#10798);
#8691=AXIS2_PLACEMENT_3D('',#13572,#10799,#10800);
#8692=AXIS2_PLACEMENT_3D('',#13574,#10801,#10802);
#8693=AXIS2_PLACEMENT_3D('',#13575,#10803,#10804);
#8694=AXIS2_PLACEMENT_3D('',#13577,#10805,#10806);
#8695=AXIS2_PLACEMENT_3D('',#13579,#10808,#10809);
#8696=AXIS2_PLACEMENT_3D('',#13581,#10810,#10811);
#8697=AXIS2_PLACEMENT_3D('',#13583,#10813,#10814);
#8698=AXIS2_PLACEMENT_3D('',#13585,#10815,#10816);
#8699=AXIS2_PLACEMENT_3D('',#13587,#10818,#10819);
#8700=AXIS2_PLACEMENT_3D('',#13589,#10820,#10821);
#8701=AXIS2_PLACEMENT_3D('',#13590,#10822,#10823);
#8702=AXIS2_PLACEMENT_3D('',#13592,#10824,#10825);
#8703=AXIS2_PLACEMENT_3D('',#13594,#10827,#10828);
#10759=DIRECTION('axis',(0.,0.,1.));
#10760=DIRECTION('refdir',(1.,0.,0.));
#10761=DIRECTION('center_axis',(0.866025403784439,0.,-0.5));
#10762=DIRECTION('ref_axis',(0.5,0.,0.866025403784439));
#10763=DIRECTION('',(-0.5,0.,-0.866025403784439));
#10764=DIRECTION('',(0.,-1.,0.));
#10765=DIRECTION('',(0.5,0.,0.866025403784439));
#10766=DIRECTION('',(0.,-1.,0.));
#10767=DIRECTION('center_axis',(1.20185167898973E-16,0.,-1.));
#10768=DIRECTION('ref_axis',(1.,0.,1.20185167898973E-16));
#10769=DIRECTION('',(-1.,0.,-1.20185167898973E-16));
#10770=DIRECTION('',(0.,-1.,0.));
#10771=DIRECTION('',(1.,0.,1.20185167898973E-16));
#10772=DIRECTION('center_axis',(-0.866025403784439,0.,-0.5));
#10773=DIRECTION('ref_axis',(0.5,0.,-0.866025403784439));
#10774=DIRECTION('',(-0.5,0.,0.866025403784439));
#10775=DIRECTION('',(0.,-1.,0.));
#10776=DIRECTION('',(0.5,0.,-0.866025403784439));
#10777=DIRECTION('center_axis',(-0.866025403784439,0.,0.5));
#10778=DIRECTION('ref_axis',(-0.5,0.,-0.866025403784439));
#10779=DIRECTION('',(0.5,0.,0.866025403784439));
#10780=DIRECTION('',(0.,-1.,0.));
#10781=DIRECTION('',(-0.5,0.,-0.866025403784439));
#10782=DIRECTION('center_axis',(-2.40370335797945E-16,0.,1.));
#10783=DIRECTION('ref_axis',(-1.,0.,-2.40370335797945E-16));
#10784=DIRECTION('',(1.,0.,2.40370335797945E-16));
#10785=DIRECTION('',(0.,-1.,0.));
#10786=DIRECTION('',(-1.,0.,-2.40370335797945E-16));
#10787=DIRECTION('center_axis',(0.866025403784439,0.,0.5));
#10788=DIRECTION('ref_axis',(-0.5,0.,0.866025403784439));
#10789=DIRECTION('',(0.5,0.,-0.866025403784439));
#10790=DIRECTION('',(-0.5,0.,0.866025403784439));
#10791=DIRECTION('center_axis',(0.,1.,0.));
#10792=DIRECTION('ref_axis',(1.,0.,0.));
#10793=DIRECTION('center_axis',(0.,-1.,0.));
#10794=DIRECTION('ref_axis',(0.,0.,-1.));
#10795=DIRECTION('center_axis',(0.,1.,0.));
#10796=DIRECTION('ref_axis',(1.,0.,0.));
#10797=DIRECTION('center_axis',(0.,1.,0.));
#10798=DIRECTION('ref_axis',(1.,0.,0.));
#10799=DIRECTION('center_axis',(0.,1.,0.));
#10800=DIRECTION('ref_axis',(0.,0.,1.));
#10801=DIRECTION('center_axis',(0.,-1.,0.));
#10802=DIRECTION('ref_axis',(1.,0.,0.));
#10803=DIRECTION('center_axis',(0.,-1.,0.));
#10804=DIRECTION('ref_axis',(1.,0.,0.));
#10805=DIRECTION('center_axis',(0.,-1.,0.));
#10806=DIRECTION('ref_axis',(1.,0.,0.));
#10807=DIRECTION('',(0.707106781186548,0.707106781186547,8.65956056235493E-17));
#10808=DIRECTION('center_axis',(0.,-1.,0.));
#10809=DIRECTION('ref_axis',(1.,0.,0.));
#10810=DIRECTION('center_axis',(0.,-1.,0.));
#10811=DIRECTION('ref_axis',(1.,0.,0.));
#10812=DIRECTION('',(0.,1.,0.));
#10813=DIRECTION('center_axis',(0.,1.,0.));
#10814=DIRECTION('ref_axis',(1.,0.,0.));
#10815=DIRECTION('center_axis',(0.,-1.,0.));
#10816=DIRECTION('ref_axis',(1.,0.,0.));
#10817=DIRECTION('',(-0.707106781186547,0.707106781186548,-8.65956056235493E-17));
#10818=DIRECTION('center_axis',(0.,-1.,0.));
#10819=DIRECTION('ref_axis',(0.,0.,-1.));
#10820=DIRECTION('center_axis',(0.,-1.,0.));
#10821=DIRECTION('ref_axis',(1.,0.,0.));
#10822=DIRECTION('center_axis',(0.,1.,0.));
#10823=DIRECTION('ref_axis',(1.,0.,0.));
#10824=DIRECTION('center_axis',(0.,1.,0.));
#10825=DIRECTION('ref_axis',(1.,0.,0.));
#10826=DIRECTION('',(-0.447213595499958,0.894427190999916,-5.47678698264203E-17));
#10827=DIRECTION('center_axis',(0.,-1.,0.));
#10828=DIRECTION('ref_axis',(1.,0.,0.));
#10829=DIRECTION('',(0.,1.,0.));
#13530=CARTESIAN_POINT('',(0.,0.,0.));
#13531=CARTESIAN_POINT('Origin',(0.115470053837925,-0.5,-0.2));
#13532=CARTESIAN_POINT('',(0.23094010767585,-0.5,0.));
#13533=CARTESIAN_POINT('',(0.115470053837925,-0.5,-0.2));
#13534=CARTESIAN_POINT('',(0.23094010767585,-0.5,0.));
#13535=CARTESIAN_POINT('',(0.115470053837925,-0.8,-0.2));
#13536=CARTESIAN_POINT('',(0.115470053837925,-0.5,-0.2));
#13537=CARTESIAN_POINT('',(0.23094010767585,-0.8,0.));
#13538=CARTESIAN_POINT('',(0.23094010767585,-0.8,0.));
#13539=CARTESIAN_POINT('',(0.23094010767585,-0.5,0.));
#13540=CARTESIAN_POINT('Origin',(-0.115470053837925,-0.5,-0.2));
#13541=CARTESIAN_POINT('',(-0.115470053837925,-0.5,-0.2));
#13542=CARTESIAN_POINT('',(0.115470053837925,-0.5,-0.2));
#13543=CARTESIAN_POINT('',(-0.115470053837925,-0.8,-0.2));
#13544=CARTESIAN_POINT('',(-0.115470053837925,-0.5,-0.2));
#13545=CARTESIAN_POINT('',(0.115470053837925,-0.8,-0.2));
#13546=CARTESIAN_POINT('Origin',(-0.23094010767585,-0.5,-2.77555756156289E-17));
#13547=CARTESIAN_POINT('',(-0.23094010767585,-0.5,-2.82820063659975E-17));
#13548=CARTESIAN_POINT('',(-0.115470053837925,-0.5,-0.2));
#13549=CARTESIAN_POINT('',(-0.23094010767585,-0.8,-2.77555756156289E-17));
#13550=CARTESIAN_POINT('',(-0.23094010767585,-0.5,-2.82820063659975E-17));
#13551=CARTESIAN_POINT('',(-0.115470053837925,-0.8,-0.2));
#13552=CARTESIAN_POINT('Origin',(-0.115470053837925,-0.5,0.2));
#13553=CARTESIAN_POINT('',(-0.115470053837925,-0.5,0.2));
#13554=CARTESIAN_POINT('',(-0.23094010767585,-0.5,-2.82820063659975E-17));
#13555=CARTESIAN_POINT('',(-0.115470053837925,-0.8,0.2));
#13556=CARTESIAN_POINT('',(-0.115470053837925,-0.5,0.2));
#13557=CARTESIAN_POINT('',(-0.23094010767585,-0.8,-2.82820063659975E-17));
#13558=CARTESIAN_POINT('Origin',(0.115470053837925,-0.5,0.2));
#13559=CARTESIAN_POINT('',(0.115470053837925,-0.5,0.2));
#13560=CARTESIAN_POINT('',(-0.115470053837925,-0.5,0.2));
#13561=CARTESIAN_POINT('',(0.115470053837925,-0.8,0.2));
#13562=CARTESIAN_POINT('',(0.115470053837925,-0.5,0.2));
#13563=CARTESIAN_POINT('',(-0.115470053837925,-0.8,0.2));
#13564=CARTESIAN_POINT('Origin',(0.23094010767585,-0.5,0.));
#13565=CARTESIAN_POINT('',(0.115470053837925,-0.5,0.2));
#13566=CARTESIAN_POINT('',(0.115470053837925,-0.8,0.2));
#13567=CARTESIAN_POINT('Origin',(0.,-0.5,0.));
#13568=CARTESIAN_POINT('Origin',(0.,-0.8,0.));
#13569=CARTESIAN_POINT('Origin',(0.,-1.4,0.));
#13570=CARTESIAN_POINT('',(-0.24505,-1.4,3.00099698131059E-17));
#13571=CARTESIAN_POINT('Origin',(0.,-1.4,0.));
#13572=CARTESIAN_POINT('Origin',(0.375,0.5,0.));
#13573=CARTESIAN_POINT('',(-0.375,0.5,-4.59242549680257E-17));
#13574=CARTESIAN_POINT('Origin',(0.,0.5,0.));
#13575=CARTESIAN_POINT('Origin',(0.,0.475,0.));
#13576=CARTESIAN_POINT('',(-0.425,0.45,-5.20474889637625E-17));
#13577=CARTESIAN_POINT('Origin',(0.,0.45,0.));
#13578=CARTESIAN_POINT('',(-0.4,0.475,-4.89858719658941E-17));
#13579=CARTESIAN_POINT('Origin',(0.,0.24,0.));
#13580=CARTESIAN_POINT('',(-0.425,0.0299999999999998,-5.20474889637625E-17));
#13581=CARTESIAN_POINT('Origin',(0.,0.0299999999999998,0.));
#13582=CARTESIAN_POINT('',(-0.425,0.24,-5.20474889637625E-17));
#13583=CARTESIAN_POINT('Origin',(0.,0.0150000000000001,0.));
#13584=CARTESIAN_POINT('',(-0.395,4.85722573273506E-17,-4.83735485663204E-17));
#13585=CARTESIAN_POINT('Origin',(0.,0.,0.));
#13586=CARTESIAN_POINT('',(-0.41,0.0150000000000001,-5.02105187650415E-17));
#13587=CARTESIAN_POINT('Origin',(0.27,0.,0.));
#13588=CARTESIAN_POINT('',(-0.27,0.,-3.30654635769785E-17));
#13589=CARTESIAN_POINT('Origin',(0.,0.,0.));
#13590=CARTESIAN_POINT('Origin',(0.,-0.02,0.));
#13591=CARTESIAN_POINT('',(-0.24505,-0.0498999999999999,3.00099698131059E-17));
#13592=CARTESIAN_POINT('Origin',(0.,-0.0498999999999999,0.));
#13593=CARTESIAN_POINT('',(-0.26,-0.02,-3.18408167778312E-17));
#13594=CARTESIAN_POINT('Origin',(0.,-0.995,0.));
#13595=CARTESIAN_POINT('',(-0.24505,-0.995,-3.00099698131059E-17));
#13780=UNCERTAINTY_MEASURE_WITH_UNIT(LENGTH_MEASURE(0.001),#13822,
'DISTANCE_ACCURACY_VALUE',
'Maximum model space distance between geometric entities at asserted c
onnectivities');
#13782=UNCERTAINTY_MEASURE_WITH_UNIT(LENGTH_MEASURE(0.001),#13822,
'DISTANCE_ACCURACY_VALUE',
'Maximum model space distance between geometric entities at asserted c
onnectivities');
#13819=(
GEOMETRIC_REPRESENTATION_CONTEXT(3)
GLOBAL_UNCERTAINTY_ASSIGNED_CONTEXT((#13780))
GLOBAL_UNIT_ASSIGNED_CONTEXT((#13822,#13824,#13825))
REPRESENTATION_CONTEXT('','3D')
);
#13821=(
GEOMETRIC_REPRESENTATION_CONTEXT(3)
GLOBAL_UNCERTAINTY_ASSIGNED_CONTEXT((#13782))
GLOBAL_UNIT_ASSIGNED_CONTEXT((#13822,#13824,#13825))
REPRESENTATION_CONTEXT('','3D')
);
#13822=(
LENGTH_UNIT()
NAMED_UNIT(*)
SI_UNIT(.CENTI.,.METRE.)
);
#13824=(
NAMED_UNIT(*)
PLANE_ANGLE_UNIT()
SI_UNIT($,.RADIAN.)
);
#13825=(
NAMED_UNIT(*)
SI_UNIT($,.STERADIAN.)
SOLID_ANGLE_UNIT()
);
#13862=SHAPE_DEFINITION_REPRESENTATION(#13905,#14032);
#13905=PRODUCT_DEFINITION_SHAPE('',$,#14071);
#14032=SHAPE_REPRESENTATION('',(#8680),#13819);
#14034=PRODUCT_DEFINITION_CONTEXT('part definition',#14150,'design');
#14071=PRODUCT_DEFINITION('M5x14 Cap Screw','M5x14 Cap Screw',#14109,#14034);
#14109=PRODUCT_DEFINITION_FORMATION('',$,#14188);
#14150=APPLICATION_CONTEXT(
'Core Data for Automotive Mechanical Design Process');
#14151=PRODUCT_CONTEXT('part definition',#14150,'mechanical');
#14188=PRODUCT('M5x14 Cap Screw','M5x14 Cap Screw','M5x14 Cap Screw',(#14151));
#14193=PRESENTATION_STYLE_ASSIGNMENT((#14198));
#14198=SURFACE_STYLE_USAGE(.BOTH.,#14203);
#14203=SURFACE_SIDE_STYLE('',(#14208));
#14208=SURFACE_STYLE_FILL_AREA(#14213);
#14213=FILL_AREA_STYLE('CAD Library Painted - Graphite',(#14218));
#14218=FILL_AREA_STYLE_COLOUR('CAD Library Painted - Graphite',#14223);
#14223=COLOUR_RGB('CAD Library Painted - Graphite',0.168627450980392,0.192156862745098,
0.231372549019608);
ENDSEC;
END-ISO-10303-21;
